ISO-10303-21;
HEADER;
FILE_DESCRIPTION (('STEP AP214'),
    '1' );
FILE_NAME ('plain washer (type a)_is_IS 2016 A- 16.step',
    '2026-10-26T19:46:16',
    ( '' ),
    ( '' ),
    'SwSTEP 2.0',
    'SolidWorks 2025',
    '' );
FILE_SCHEMA (( 'AUTOMOTIVE_DESIGN' ));
ENDSEC;

DATA;
#74=AXIS2_PLACEMENT_3D ( 'NONE', #50594, #44950, #67957 ) ;
#634=CARTESIAN_POINT ( 'NONE',  ( 0.000000000000000000, 0.000000000000000000, 0.000000000000000000 ) ) ;
#1235=CARTESIAN_POINT ( 'NONE',  ( 1.714505518806294638E-15, 0.000000000000000000, -14.00000000000000000 ) ) ;
#1433=CARTESIAN_POINT ( 'NONE',  ( 0.000000000000000000, -2.500000000000000444, 0.000000000000000000 ) ) ;
#1435=APPLICATION_CONTEXT ( 'automotive_design' ) ;
#2008=PLANE ( 'NONE',  #70655 ) ;
#2757=EDGE_CURVE ( 'NONE', #64164, #35360, #7508, .T. ) ;
#2821=DIRECTION ( 'NONE',  ( -0.000000000000000000, 1.000000000000000000, -0.000000000000000000 ) ) ;
#3443=EDGE_LOOP ( 'NONE', ( #34992, #24925 ) ) ;
#3465=PLANE ( 'NONE',  #74 ) ;
#4020=FACE_OUTER_BOUND ( 'NONE', #58733, .T. ) ;
#4591=FACE_BOUND ( 'NONE', #5914, .T. ) ;
#4704=DIRECTION ( 'NONE',  ( 0.000000000000000000, 0.000000000000000000, 1.000000000000000000 ) ) ;
#4730=EDGE_CURVE ( 'NONE', #17458, #33763, #57876, .T. ) ;
#4921=ADVANCED_FACE ( 'NONE', ( #4020 ), #9293, .F. ) ;
#5552=AXIS2_PLACEMENT_3D ( 'NONE', #52530, #34086, #40094 ) ;
#5820=ORIENTED_EDGE ( 'NONE', *, *, #9926, .T. ) ;
#5914=EDGE_LOOP ( 'NONE', ( #18227, #52514 ) ) ;
#6441=VECTOR ( 'NONE', #18018, 1000.000000000000000 ) ;
#7508=CIRCLE ( 'NONE', #49658, 8.000000000000000000 ) ;
#7676=ORIENTED_EDGE ( 'NONE', *, *, #68773, .T. ) ;
#7817=ORIENTED_EDGE ( 'NONE', *, *, #48596, .T. ) ;
#8107=DIRECTION ( 'NONE',  ( 0.000000000000000000, 0.000000000000000000, 1.000000000000000000 ) ) ;
#8206=ADVANCED_FACE ( 'NONE', ( #11189 ), #29651, .T. ) ;
#9293=CYLINDRICAL_SURFACE ( 'NONE', #9724, 8.000000000000000000 ) ;
#9724=AXIS2_PLACEMENT_3D ( 'NONE', #27752, #61722, #32316 ) ;
#9926=EDGE_CURVE ( 'NONE', #68962, #53267, #42596, .T. ) ;
#9931=ORIENTED_EDGE ( 'NONE', *, *, #45089, .T. ) ;
#10485=PRODUCT_DEFINITION_FORMATION_WITH_SPECIFIED_SOURCE ( 'ANY', '', #20355, .NOT_KNOWN. ) ;
#10707=ORIENTED_EDGE ( 'NONE', *, *, #59477, .F. ) ;
#10870=LINE ( 'NONE', #69328, #6441 ) ;
#11109=CARTESIAN_POINT ( 'NONE',  ( 1.714505518806294638E-15, -2.500000000000000444, -14.00000000000000000 ) ) ;
#11189=FACE_OUTER_BOUND ( 'NONE', #66898, .T. ) ;
#11422=DIRECTION ( 'NONE',  ( 0.000000000000000000, 0.000000000000000000, 1.000000000000000000 ) ) ;
#11835=CIRCLE ( 'NONE', #56428, 14.00000000000000000 ) ;
#13462=ADVANCED_FACE ( 'NONE', ( #56272, #4591 ), #3465, .T. ) ;
#13545=EDGE_CURVE ( 'NONE', #35360, #19306, #48229, .T. ) ;
#13817=CARTESIAN_POINT ( 'NONE',  ( 9.797174393178825657E-16, 0.000000000000000000, -8.000000000000000000 ) ) ;
#14879=FACE_OUTER_BOUND ( 'NONE', #31412, .T. ) ;
#14952=ADVANCED_FACE ( 'NONE', ( #27504 ), #32441, .T. ) ;
#15011=DIRECTION ( 'NONE',  ( -0.000000000000000000, 1.000000000000000000, -0.000000000000000000 ) ) ;
#15061=DIRECTION ( 'NONE',  ( -0.000000000000000000, 1.000000000000000000, -0.000000000000000000 ) ) ;
#16871=PRODUCT_DEFINITION_CONTEXT ( 'detailed design', #1435, 'design' ) ;
#16884=VECTOR ( 'NONE', #15011, 1000.000000000000000 ) ;
#17458=VERTEX_POINT ( 'NONE', #11109 ) ;
#17543=ORIENTED_EDGE ( 'NONE', *, *, #13545, .T. ) ;
#17583=DIRECTION ( 'NONE',  ( 0.000000000000000000, 0.000000000000000000, 1.000000000000000000 ) ) ;
#17825=EDGE_LOOP ( 'NONE', ( #59764, #5820 ) ) ;
#18018=DIRECTION ( 'NONE',  ( -0.000000000000000000, 1.000000000000000000, -0.000000000000000000 ) ) ;
#18227=ORIENTED_EDGE ( 'NONE', *, *, #59819, .F. ) ;
#19306=VERTEX_POINT ( 'NONE', #23048 ) ;
#19402=( LENGTH_UNIT ( ) NAMED_UNIT ( * ) SI_UNIT ( .MILLI., .METRE. ) );
#19556=CIRCLE ( 'NONE', #38871, 14.00000000000000000 ) ;
#20355=PRODUCT ( 'plain washer (type a)_is_IS 2016 A- 16', 'plain washer (type a)_is_IS 2016 A- 16', '', ( #62175 ) ) ;
#20701=CARTESIAN_POINT ( 'NONE',  ( 0.000000000000000000, 0.000000000000000000, 0.000000000000000000 ) ) ;
#20753=VECTOR ( 'NONE', #50336, 1000.000000000000000 ) ;
#21456=ORIENTED_EDGE ( 'NONE', *, *, #57024, .F. ) ;
#21600=DIRECTION ( 'NONE',  ( 0.000000000000000000, 0.000000000000000000, 1.000000000000000000 ) ) ;
#23048=CARTESIAN_POINT ( 'NONE',  ( 0.000000000000000000, 0.000000000000000000, 8.000000000000000000 ) ) ;
#23253=EDGE_LOOP ( 'NONE', ( #21456, #41919, #7817, #42586 ) ) ;
#23907=FACE_OUTER_BOUND ( 'NONE', #26201, .T. ) ;
#24093=CARTESIAN_POINT ( 'NONE',  ( 0.000000000000000000, -2.500000000000000444, 14.00000000000000000 ) ) ;
#24546=ADVANCED_BREP_SHAPE_REPRESENTATION ( '', ( #67054, #57354 ), #57409 ) ;
#24635=CARTESIAN_POINT ( 'NONE',  ( 8.000000000000000000, -2.500000000000000444, 0.000000000000000000 ) ) ;
#24925=ORIENTED_EDGE ( 'NONE', *, *, #2757, .T. ) ;
#25739=AXIS2_PLACEMENT_3D ( 'NONE', #37906, #2821, #8107 ) ;
#26036=ORIENTED_EDGE ( 'NONE', *, *, #59819, .T. ) ;
#26086=PRODUCT_DEFINITION ( 'UNKNOWN', '', #10485, #16871 ) ;
#26201=EDGE_LOOP ( 'NONE', ( #32883, #56512 ) ) ;
#26964=CARTESIAN_POINT ( 'NONE',  ( 0.000000000000000000, -2.500000000000000444, 0.000000000000000000 ) ) ;
#27504=FACE_OUTER_BOUND ( 'NONE', #23253, .T. ) ;
#27752=CARTESIAN_POINT ( 'NONE',  ( 0.000000000000000000, 0.000000000000000000, 0.000000000000000000 ) ) ;
#28678=AXIS2_PLACEMENT_3D ( 'NONE', #69070, #35127, #58142 ) ;
#29053=SHAPE_REPRESENTATION_RELATIONSHIP ( 'NONE' , 'NONE' ,  #66708, #24546 ) ;
#29651=CYLINDRICAL_SURFACE ( 'NONE', #64273, 14.00000000000000000 ) ;
#31257=CIRCLE ( 'NONE', #28678, 8.000000000000000000 ) ;
#31412=EDGE_LOOP ( 'NONE', ( #55987, #65523, #7676, #64639 ) ) ;
#31659=DIRECTION ( 'NONE',  ( 0.000000000000000000, 0.000000000000000000, 1.000000000000000000 ) ) ;
#32260=CARTESIAN_POINT ( 'NONE',  ( 0.000000000000000000, 0.000000000000000000, 14.00000000000000000 ) ) ;
#32316=DIRECTION ( 'NONE',  ( 0.000000000000000000, 0.000000000000000000, 1.000000000000000000 ) ) ;
#32441=CYLINDRICAL_SURFACE ( 'NONE', #44700, 14.00000000000000000 ) ;
#32883=ORIENTED_EDGE ( 'NONE', *, *, #45089, .F. ) ;
#33763=VERTEX_POINT ( 'NONE', #24093 ) ;
#34086=DIRECTION ( 'NONE',  ( -0.000000000000000000, 1.000000000000000000, -0.000000000000000000 ) ) ;
#34459=DIRECTION ( 'NONE',  ( 1.000000000000000000, 0.000000000000000000, 0.000000000000000000 ) ) ;
#34740=( NAMED_UNIT ( * ) SI_UNIT ( $, .STERADIAN. ) SOLID_ANGLE_UNIT ( ) );
#34992=ORIENTED_EDGE ( 'NONE', *, *, #52416, .T. ) ;
#35127=DIRECTION ( 'NONE',  ( -0.000000000000000000, 1.000000000000000000, -0.000000000000000000 ) ) ;
#35320=CIRCLE ( 'NONE', #54577, 8.000000000000000000 ) ;
#35360=VERTEX_POINT ( 'NONE', #42879 ) ;
#36398=ADVANCED_FACE ( 'NONE', ( #41266, #23907 ), #2008, .T. ) ;
#36854=DIRECTION ( 'NONE',  ( 0.000000000000000000, 0.000000000000000000, 1.000000000000000000 ) ) ;
#37906=CARTESIAN_POINT ( 'NONE',  ( 0.000000000000000000, 0.000000000000000000, 0.000000000000000000 ) ) ;
#37918=CYLINDRICAL_SURFACE ( 'NONE', #72562, 8.000000000000000000 ) ;
#37964=( GEOMETRIC_REPRESENTATION_CONTEXT ( 3 ) GLOBAL_UNCERTAINTY_ASSIGNED_CONTEXT ( ( #52616 ) ) GLOBAL_UNIT_ASSIGNED_CONTEXT ( ( #19402, #59055, #53755 ) ) REPRESENTATION_CONTEXT ( 'NONE', 'WORKASPACE' ) );
#38600=ORIENTED_EDGE ( 'NONE', *, *, #57024, .T. ) ;
#38871=AXIS2_PLACEMENT_3D ( 'NONE', #26964, #55287, #49980 ) ;
#39449=CARTESIAN_POINT ( 'NONE',  ( 0.000000000000000000, 0.000000000000000000, 14.00000000000000000 ) ) ;
#40094=DIRECTION ( 'NONE',  ( 0.000000000000000000, 0.000000000000000000, 1.000000000000000000 ) ) ;
#41266=FACE_BOUND ( 'NONE', #3443, .T. ) ;
#41919=ORIENTED_EDGE ( 'NONE', *, *, #4730, .T. ) ;
#42015=CARTESIAN_POINT ( 'NONE',  ( 9.797174393178825657E-16, -2.500000000000000444, -8.000000000000000000 ) ) ;
#42586=ORIENTED_EDGE ( 'NONE', *, *, #9926, .F. ) ;
#42596=CIRCLE ( 'NONE', #25739, 14.00000000000000000 ) ;
#42879=CARTESIAN_POINT ( 'NONE',  ( 0.000000000000000000, -2.500000000000000444, 8.000000000000000000 ) ) ;
#43039=CLOSED_SHELL ( 'NONE', ( #8206, #48657, #4921, #13462, #14952, #36398 ) ) ;
#43434=LINE ( 'NONE', #44569, #44570 ) ;
#43719=DIRECTION ( 'NONE',  ( -0.000000000000000000, 1.000000000000000000, -0.000000000000000000 ) ) ;
#43879=PRODUCT_DEFINITION_SHAPE ( 'NONE', 'NONE',  #26086 ) ;
#44569=CARTESIAN_POINT ( 'NONE',  ( 1.714505518806294638E-15, 0.000000000000000000, -14.00000000000000000 ) ) ;
#44570=VECTOR ( 'NONE', #60418, 1000.000000000000000 ) ;
#44700=AXIS2_PLACEMENT_3D ( 'NONE', #67508, #15061, #44870 ) ;
#44870=DIRECTION ( 'NONE',  ( 0.000000000000000000, 0.000000000000000000, 1.000000000000000000 ) ) ;
#44950=DIRECTION ( 'NONE',  ( -0.000000000000000000, 1.000000000000000000, 0.000000000000000000 ) ) ;
#45089=EDGE_CURVE ( 'NONE', #33763, #17458, #19556, .T. ) ;
#48229=LINE ( 'NONE', #71604, #16884 ) ;
#48596=EDGE_CURVE ( 'NONE', #33763, #53267, #62035, .T. ) ;
#48657=ADVANCED_FACE ( 'NONE', ( #14879 ), #37918, .F. ) ;
#49523=DIRECTION ( 'NONE',  ( 0.000000000000000000, 0.000000000000000000, 1.000000000000000000 ) ) ;
#49658=AXIS2_PLACEMENT_3D ( 'NONE', #67633, #60845, #49523 ) ;
#49980=DIRECTION ( 'NONE',  ( 0.000000000000000000, 0.000000000000000000, 1.000000000000000000 ) ) ;
#50336=DIRECTION ( 'NONE',  ( -0.000000000000000000, 1.000000000000000000, -0.000000000000000000 ) ) ;
#50570=( LENGTH_UNIT ( ) NAMED_UNIT ( * ) SI_UNIT ( .MILLI., .METRE. ) );
#50594=CARTESIAN_POINT ( 'NONE',  ( 8.000000000000000000, 0.000000000000000000, 0.000000000000000000 ) ) ;
#52416=EDGE_CURVE ( 'NONE', #35360, #64164, #35320, .T. ) ;
#52514=ORIENTED_EDGE ( 'NONE', *, *, #68773, .F. ) ;
#52530=CARTESIAN_POINT ( 'NONE',  ( 0.000000000000000000, 0.000000000000000000, 0.000000000000000000 ) ) ;
#52616=UNCERTAINTY_MEASURE_WITH_UNIT (LENGTH_MEASURE( 1.000000000000000082E-05 ), #19402, 'distance_accuracy_value', 'NONE');
#52840=EDGE_CURVE ( 'NONE', #64164, #66501, #10870, .T. ) ;
#53188=UNCERTAINTY_MEASURE_WITH_UNIT (LENGTH_MEASURE( 1.000000000000000082E-05 ), #50570, 'distance_accuracy_value', 'NONE');
#53267=VERTEX_POINT ( 'NONE', #39449 ) ;
#53755=( NAMED_UNIT ( * ) SI_UNIT ( $, .STERADIAN. ) SOLID_ANGLE_UNIT ( ) );
#54577=AXIS2_PLACEMENT_3D ( 'NONE', #67270, #66891, #21600 ) ;
#55287=DIRECTION ( 'NONE',  ( -0.000000000000000000, 1.000000000000000000, -0.000000000000000000 ) ) ;
#55987=ORIENTED_EDGE ( 'NONE', *, *, #2757, .F. ) ;
#56272=FACE_OUTER_BOUND ( 'NONE', #17825, .T. ) ;
#56428=AXIS2_PLACEMENT_3D ( 'NONE', #20701, #43719, #31659 ) ;
#56512=ORIENTED_EDGE ( 'NONE', *, *, #4730, .F. ) ;
#56994=( NAMED_UNIT ( * ) PLANE_ANGLE_UNIT ( ) SI_UNIT ( $, .RADIAN. ) );
#57024=EDGE_CURVE ( 'NONE', #17458, #68962, #43434, .T. ) ;
#57354=AXIS2_PLACEMENT_3D ( 'NONE', #63097, #11422, #34459 ) ;
#57409=( GEOMETRIC_REPRESENTATION_CONTEXT ( 3 ) GLOBAL_UNCERTAINTY_ASSIGNED_CONTEXT ( ( #53188 ) ) GLOBAL_UNIT_ASSIGNED_CONTEXT ( ( #50570, #56994, #34740 ) ) REPRESENTATION_CONTEXT ( 'NONE', 'WORKASPACE' ) );
#57515=DIRECTION ( 'NONE',  ( -0.000000000000000000, 1.000000000000000000, -0.000000000000000000 ) ) ;
#57876=CIRCLE ( 'NONE', #67490, 14.00000000000000000 ) ;
#57976=DIRECTION ( 'NONE',  ( -0.000000000000000000, 1.000000000000000000, -0.000000000000000000 ) ) ;
#58142=DIRECTION ( 'NONE',  ( 0.000000000000000000, 0.000000000000000000, 1.000000000000000000 ) ) ;
#58733=EDGE_LOOP ( 'NONE', ( #58817, #65779, #17543, #26036 ) ) ;
#58817=ORIENTED_EDGE ( 'NONE', *, *, #52840, .F. ) ;
#59055=( NAMED_UNIT ( * ) PLANE_ANGLE_UNIT ( ) SI_UNIT ( $, .RADIAN. ) );
#59477=EDGE_CURVE ( 'NONE', #53267, #68962, #11835, .T. ) ;
#59764=ORIENTED_EDGE ( 'NONE', *, *, #59477, .T. ) ;
#59819=EDGE_CURVE ( 'NONE', #19306, #66501, #31257, .T. ) ;
#60418=DIRECTION ( 'NONE',  ( -0.000000000000000000, 1.000000000000000000, -0.000000000000000000 ) ) ;
#60845=DIRECTION ( 'NONE',  ( -0.000000000000000000, 1.000000000000000000, -0.000000000000000000 ) ) ;
#60915=CARTESIAN_POINT ( 'NONE',  ( 0.000000000000000000, 0.000000000000000000, 0.000000000000000000 ) ) ;
#61722=DIRECTION ( 'NONE',  ( -0.000000000000000000, 1.000000000000000000, -0.000000000000000000 ) ) ;
#62035=LINE ( 'NONE', #32260, #20753 ) ;
#62175=PRODUCT_CONTEXT ( 'NONE', #69837, 'mechanical' ) ;
#62330=ORIENTED_EDGE ( 'NONE', *, *, #48596, .F. ) ;
#63097=CARTESIAN_POINT ( 'NONE',  ( 0.000000000000000000, 0.000000000000000000, 0.000000000000000000 ) ) ;
#64164=VERTEX_POINT ( 'NONE', #42015 ) ;
#64273=AXIS2_PLACEMENT_3D ( 'NONE', #634, #57976, #17583 ) ;
#64639=ORIENTED_EDGE ( 'NONE', *, *, #13545, .F. ) ;
#65523=ORIENTED_EDGE ( 'NONE', *, *, #52840, .T. ) ;
#65779=ORIENTED_EDGE ( 'NONE', *, *, #52416, .F. ) ;
#66501=VERTEX_POINT ( 'NONE', #13817 ) ;
#66708=SHAPE_REPRESENTATION ( 'plain washer (type a)_is_IS 2016 A- 16', ( #57354 ), #57409 ) ;
#66877=STYLED_ITEM('',(#74706),#67054);
#66891=DIRECTION ( 'NONE',  ( -0.000000000000000000, 1.000000000000000000, -0.000000000000000000 ) ) ;
#66898=EDGE_LOOP ( 'NONE', ( #9931, #38600, #10707, #62330 ) ) ;
#67054=MANIFOLD_SOLID_BREP ( 'BaseBody', #43039 ) ;
#67270=CARTESIAN_POINT ( 'NONE',  ( 0.000000000000000000, -2.500000000000000444, 0.000000000000000000 ) ) ;
#67490=AXIS2_PLACEMENT_3D ( 'NONE', #1433, #71530, #36854 ) ;
#67508=CARTESIAN_POINT ( 'NONE',  ( 0.000000000000000000, 0.000000000000000000, 0.000000000000000000 ) ) ;
#67633=CARTESIAN_POINT ( 'NONE',  ( 0.000000000000000000, -2.500000000000000444, 0.000000000000000000 ) ) ;
#67957=DIRECTION ( 'NONE',  ( 0.000000000000000000, 0.000000000000000000, 1.000000000000000000 ) ) ;
#68773=EDGE_CURVE ( 'NONE', #66501, #19306, #70590, .T. ) ;
#68962=VERTEX_POINT ( 'NONE', #1235 ) ;
#69070=CARTESIAN_POINT ( 'NONE',  ( 0.000000000000000000, 0.000000000000000000, 0.000000000000000000 ) ) ;
#69328=CARTESIAN_POINT ( 'NONE',  ( 9.797174393178825657E-16, 0.000000000000000000, -8.000000000000000000 ) ) ;
#69837=APPLICATION_CONTEXT ( 'automotive_design' ) ;
#69942=DIRECTION ( 'NONE',  ( 0.000000000000000000, -0.000000000000000000, -1.000000000000000000 ) ) ;
#70529=MECHANICAL_DESIGN_GEOMETRIC_PRESENTATION_REPRESENTATION('',(#66877),#37964);
#70590=CIRCLE ( 'NONE', #5552, 8.000000000000000000 ) ;
#70655=AXIS2_PLACEMENT_3D ( 'NONE', #24635, #70668, #69942 ) ;
#70668=DIRECTION ( 'NONE',  ( 0.000000000000000000, -1.000000000000000000, 0.000000000000000000 ) ) ;
#71530=DIRECTION ( 'NONE',  ( -0.000000000000000000, 1.000000000000000000, -0.000000000000000000 ) ) ;
#71604=CARTESIAN_POINT ( 'NONE',  ( 0.000000000000000000, 0.000000000000000000, 8.000000000000000000 ) ) ;
#72562=AXIS2_PLACEMENT_3D ( 'NONE', #60915, #57515, #4704 ) ;
#73872=SHAPE_DEFINITION_REPRESENTATION ( #43879, #66708 ) ;
#74700=COLOUR_RGB('Black',0.12,0.14,0.17);
#74701=FILL_AREA_STYLE_COLOUR('',#74700);
#74702=FILL_AREA_STYLE('',(#74701));
#74703=SURFACE_STYLE_FILL_AREA(#74702);
#74704=SURFACE_SIDE_STYLE('',(#74703));
#74705=SURFACE_STYLE_USAGE(.BOTH.,#74704);
#74706=PRESENTATION_STYLE_ASSIGNMENT((#74705));
ENDSEC;
END-ISO-10303-21;
